ISO-10303-21;
HEADER;
/* Generated by software containing ST-Developer
 * from STEP Tools, Inc. (www.steptools.com) 
 */

FILE_DESCRIPTION(
/* description */ ('Over-Centre Plunger Toggle Clamp on Slotted Fixture Frame'),
/* implementation_level */ '2;1');

FILE_NAME(
/* name */ 
'M5x14 Cap Screw.step',
/* time_stamp */ '2026-10-28T03:23:24-07:00',
/* author */ (''),
/* organization */ (''),
/* preprocessor_version */ 'ST-DEVELOPER v20.2',
/* originating_system */ 'Autodesk Translation Framework v15.17.0.0',
/* authorisation */ '');

FILE_SCHEMA (('AUTOMOTIVE_DESIGN { 1 0 10303 214 3 1 1 }'));
ENDSEC;

DATA;
#10=MECHANICAL_DESIGN_GEOMETRIC_PRESENTATION_REPRESENTATION('',(#528),#15212);
#397=ORIENTED_CLOSED_SHELL('',*,#8260,.F.);
#401=BREP_WITH_VOIDS('Body1',#8261,(#397));
#406=CONICAL_SURFACE('',#9153,0.4,0.785398163397448);
#407=CONICAL_SURFACE('',#9157,0.41,0.785398163397448);
#408=CONICAL_SURFACE('',#9161,0.26,0.463647609000806);
#444=SHAPE_REPRESENTATION_RELATIONSHIP('SRR','None',#15418,#486);
#486=ADVANCED_BREP_SHAPE_REPRESENTATION('',(#401),#15180);
#528=STYLED_ITEM('',(#15726),#401);
#719=FACE_BOUND('',#1910,.T.);
#927=PLANE('',#9141);
#928=PLANE('',#9142);
#929=PLANE('',#9143);
#930=PLANE('',#9144);
#931=PLANE('',#9145);
#932=PLANE('',#9146);
#933=PLANE('',#9147);
#934=PLANE('',#9148);
#935=PLANE('',#9149);
#936=PLANE('',#9151);
#937=PLANE('',#9159);
#1302=FACE_OUTER_BOUND('',#1896,.T.);
#1303=FACE_OUTER_BOUND('',#1897,.T.);
#1304=FACE_OUTER_BOUND('',#1898,.T.);
#1305=FACE_OUTER_BOUND('',#1899,.T.);
#1306=FACE_OUTER_BOUND('',#1900,.T.);
#1307=FACE_OUTER_BOUND('',#1901,.T.);
#1308=FACE_OUTER_BOUND('',#1902,.T.);
#1309=FACE_OUTER_BOUND('',#1903,.T.);
#1310=FACE_OUTER_BOUND('',#1904,.T.);
#1311=FACE_OUTER_BOUND('',#1905,.T.);
#1312=FACE_OUTER_BOUND('',#1906,.T.);
#1313=FACE_OUTER_BOUND('',#1907,.T.);
#1314=FACE_OUTER_BOUND('',#1908,.T.);
#1315=FACE_OUTER_BOUND('',#1909,.T.);
#1316=FACE_OUTER_BOUND('',#1911,.T.);
#1317=FACE_OUTER_BOUND('',#1912,.T.);
#1896=EDGE_LOOP('',(#6569,#6570,#6571,#6572));
#1897=EDGE_LOOP('',(#6573,#6574,#6575,#6576));
#1898=EDGE_LOOP('',(#6577,#6578,#6579,#6580));
#1899=EDGE_LOOP('',(#6581,#6582,#6583,#6584));
#1900=EDGE_LOOP('',(#6585,#6586,#6587,#6588));
#1901=EDGE_LOOP('',(#6589,#6590,#6591,#6592));
#1902=EDGE_LOOP('',(#6593,#6594,#6595,#6596,#6597,#6598));
#1903=EDGE_LOOP('',(#6599,#6600,#6601,#6602,#6603,#6604));
#1904=EDGE_LOOP('',(#6605));
#1905=EDGE_LOOP('',(#6606));
#1906=EDGE_LOOP('',(#6607,#6608,#6609,#6610));
#1907=EDGE_LOOP('',(#6611,#6612,#6613,#6614));
#1908=EDGE_LOOP('',(#6615,#6616,#6617,#6618));
#1909=EDGE_LOOP('',(#6619));
#1910=EDGE_LOOP('',(#6620));
#1911=EDGE_LOOP('',(#6621,#6622,#6623,#6624));
#1912=EDGE_LOOP('',(#6625,#6626,#6627,#6628));
#2586=LINE('',#13435,#3216);
#2587=LINE('',#13437,#3217);
#2588=LINE('',#13439,#3218);
#2589=LINE('',#13440,#3219);
#2590=LINE('',#13443,#3220);
#2591=LINE('',#13445,#3221);
#2592=LINE('',#13446,#3222);
#2593=LINE('',#13449,#3223);
#2594=LINE('',#13451,#3224);
#2595=LINE('',#13452,#3225);
#2596=LINE('',#13455,#3226);
#2597=LINE('',#13457,#3227);
#2598=LINE('',#13458,#3228);
#2599=LINE('',#13461,#3229);
#2600=LINE('',#13463,#3230);
#2601=LINE('',#13464,#3231);
#2602=LINE('',#13466,#3232);
#2603=LINE('',#13467,#3233);
#2604=LINE('',#13479,#3234);
#2605=LINE('',#13483,#3235);
#2606=LINE('',#13487,#3236);
#2607=LINE('',#13494,#3237);
#2608=LINE('',#13496,#3238);
#3216=VECTOR('',#10867,1.);
#3217=VECTOR('',#10868,1.);
#3218=VECTOR('',#10869,1.);
#3219=VECTOR('',#10870,1.);
#3220=VECTOR('',#10873,1.);
#3221=VECTOR('',#10874,1.);
#3222=VECTOR('',#10875,1.);
#3223=VECTOR('',#10878,1.);
#3224=VECTOR('',#10879,1.);
#3225=VECTOR('',#10880,1.);
#3226=VECTOR('',#10883,1.);
#3227=VECTOR('',#10884,1.);
#3228=VECTOR('',#10885,1.);
#3229=VECTOR('',#10888,1.);
#3230=VECTOR('',#10889,1.);
#3231=VECTOR('',#10890,1.);
#3232=VECTOR('',#10893,1.);
#3233=VECTOR('',#10894,1.);
#3234=VECTOR('',#10911,0.4);
#3235=VECTOR('',#10916,0.425);
#3236=VECTOR('',#10921,0.41);
#3237=VECTOR('',#10930,0.26);
#3238=VECTOR('',#10933,0.25);
#3634=CIRCLE('',#9150,0.24505);
#3635=CIRCLE('',#9152,0.375);
#3636=CIRCLE('',#9154,0.425);
#3637=CIRCLE('',#9156,0.425);
#3638=CIRCLE('',#9158,0.395);
#3639=CIRCLE('',#9160,0.27);
#3640=CIRCLE('',#9162,0.24505);
#4192=VERTEX_POINT('',#13433);
#4193=VERTEX_POINT('',#13434);
#4194=VERTEX_POINT('',#13436);
#4195=VERTEX_POINT('',#13438);
#4196=VERTEX_POINT('',#13442);
#4197=VERTEX_POINT('',#13444);
#4198=VERTEX_POINT('',#13448);
#4199=VERTEX_POINT('',#13450);
#4200=VERTEX_POINT('',#13454);
#4201=VERTEX_POINT('',#13456);
#4202=VERTEX_POINT('',#13460);
#4203=VERTEX_POINT('',#13462);
#4204=VERTEX_POINT('',#13471);
#4205=VERTEX_POINT('',#13474);
#4206=VERTEX_POINT('',#13477);
#4207=VERTEX_POINT('',#13481);
#4208=VERTEX_POINT('',#13485);
#4209=VERTEX_POINT('',#13489);
#4210=VERTEX_POINT('',#13492);
#5045=EDGE_CURVE('',#4192,#4193,#2586,.T.);
#5046=EDGE_CURVE('',#4193,#4194,#2587,.T.);
#5047=EDGE_CURVE('',#4194,#4195,#2588,.T.);
#5048=EDGE_CURVE('',#4192,#4195,#2589,.T.);
#5049=EDGE_CURVE('',#4193,#4196,#2590,.T.);
#5050=EDGE_CURVE('',#4196,#4197,#2591,.T.);
#5051=EDGE_CURVE('',#4197,#4194,#2592,.T.);
#5052=EDGE_CURVE('',#4196,#4198,#2593,.T.);
#5053=EDGE_CURVE('',#4198,#4199,#2594,.T.);
#5054=EDGE_CURVE('',#4199,#4197,#2595,.T.);
#5055=EDGE_CURVE('',#4198,#4200,#2596,.T.);
#5056=EDGE_CURVE('',#4200,#4201,#2597,.T.);
#5057=EDGE_CURVE('',#4201,#4199,#2598,.T.);
#5058=EDGE_CURVE('',#4200,#4202,#2599,.T.);
#5059=EDGE_CURVE('',#4202,#4203,#2600,.T.);
#5060=EDGE_CURVE('',#4203,#4201,#2601,.T.);
#5061=EDGE_CURVE('',#4202,#4192,#2602,.T.);
#5062=EDGE_CURVE('',#4195,#4203,#2603,.T.);
#5063=EDGE_CURVE('',#4204,#4204,#3634,.T.);
#5064=EDGE_CURVE('',#4205,#4205,#3635,.T.);
#5065=EDGE_CURVE('',#4206,#4206,#3636,.T.);
#5066=EDGE_CURVE('',#4206,#4205,#2604,.T.);
#5067=EDGE_CURVE('',#4207,#4207,#3637,.T.);
#5068=EDGE_CURVE('',#4207,#4206,#2605,.T.);
#5069=EDGE_CURVE('',#4208,#4208,#3638,.T.);
#5070=EDGE_CURVE('',#4208,#4207,#2606,.T.);
#5071=EDGE_CURVE('',#4209,#4209,#3639,.T.);
#5072=EDGE_CURVE('',#4210,#4210,#3640,.F.);
#5073=EDGE_CURVE('',#4210,#4209,#2607,.T.);
#5074=EDGE_CURVE('',#4204,#4210,#2608,.T.);
#6569=ORIENTED_EDGE('',*,*,#5045,.T.);
#6570=ORIENTED_EDGE('',*,*,#5046,.T.);
#6571=ORIENTED_EDGE('',*,*,#5047,.T.);
#6572=ORIENTED_EDGE('',*,*,#5048,.F.);
#6573=ORIENTED_EDGE('',*,*,#5049,.T.);
#6574=ORIENTED_EDGE('',*,*,#5050,.T.);
#6575=ORIENTED_EDGE('',*,*,#5051,.T.);
#6576=ORIENTED_EDGE('',*,*,#5046,.F.);
#6577=ORIENTED_EDGE('',*,*,#5052,.T.);
#6578=ORIENTED_EDGE('',*,*,#5053,.T.);
#6579=ORIENTED_EDGE('',*,*,#5054,.T.);
#6580=ORIENTED_EDGE('',*,*,#5050,.F.);
#6581=ORIENTED_EDGE('',*,*,#5055,.T.);
#6582=ORIENTED_EDGE('',*,*,#5056,.T.);
#6583=ORIENTED_EDGE('',*,*,#5057,.T.);
#6584=ORIENTED_EDGE('',*,*,#5053,.F.);
#6585=ORIENTED_EDGE('',*,*,#5058,.T.);
#6586=ORIENTED_EDGE('',*,*,#5059,.T.);
#6587=ORIENTED_EDGE('',*,*,#5060,.T.);
#6588=ORIENTED_EDGE('',*,*,#5056,.F.);
#6589=ORIENTED_EDGE('',*,*,#5061,.T.);
#6590=ORIENTED_EDGE('',*,*,#5048,.T.);
#6591=ORIENTED_EDGE('',*,*,#5062,.T.);
#6592=ORIENTED_EDGE('',*,*,#5059,.F.);
#6593=ORIENTED_EDGE('',*,*,#5061,.F.);
#6594=ORIENTED_EDGE('',*,*,#5058,.F.);
#6595=ORIENTED_EDGE('',*,*,#5055,.F.);
#6596=ORIENTED_EDGE('',*,*,#5052,.F.);
#6597=ORIENTED_EDGE('',*,*,#5049,.F.);
#6598=ORIENTED_EDGE('',*,*,#5045,.F.);
#6599=ORIENTED_EDGE('',*,*,#5062,.F.);
#6600=ORIENTED_EDGE('',*,*,#5047,.F.);
#6601=ORIENTED_EDGE('',*,*,#5051,.F.);
#6602=ORIENTED_EDGE('',*,*,#5054,.F.);
#6603=ORIENTED_EDGE('',*,*,#5057,.F.);
#6604=ORIENTED_EDGE('',*,*,#5060,.F.);
#6605=ORIENTED_EDGE('',*,*,#5063,.F.);
#6606=ORIENTED_EDGE('',*,*,#5064,.F.);
#6607=ORIENTED_EDGE('',*,*,#5065,.F.);
#6608=ORIENTED_EDGE('',*,*,#5066,.T.);
#6609=ORIENTED_EDGE('',*,*,#5064,.T.);
#6610=ORIENTED_EDGE('',*,*,#5066,.F.);
#6611=ORIENTED_EDGE('',*,*,#5067,.F.);
#6612=ORIENTED_EDGE('',*,*,#5068,.T.);
#6613=ORIENTED_EDGE('',*,*,#5065,.T.);
#6614=ORIENTED_EDGE('',*,*,#5068,.F.);
#6615=ORIENTED_EDGE('',*,*,#5069,.F.);
#6616=ORIENTED_EDGE('',*,*,#5070,.T.);
#6617=ORIENTED_EDGE('',*,*,#5067,.T.);
#6618=ORIENTED_EDGE('',*,*,#5070,.F.);
#6619=ORIENTED_EDGE('',*,*,#5069,.T.);
#6620=ORIENTED_EDGE('',*,*,#5071,.F.);
#6621=ORIENTED_EDGE('',*,*,#5072,.F.);
#6622=ORIENTED_EDGE('',*,*,#5073,.T.);
#6623=ORIENTED_EDGE('',*,*,#5071,.T.);
#6624=ORIENTED_EDGE('',*,*,#5073,.F.);
#6625=ORIENTED_EDGE('',*,*,#5063,.T.);
#6626=ORIENTED_EDGE('',*,*,#5074,.T.);
#6627=ORIENTED_EDGE('',*,*,#5072,.T.);
#6628=ORIENTED_EDGE('',*,*,#5074,.F.);
#7687=CYLINDRICAL_SURFACE('',#9155,0.425);
#7688=CYLINDRICAL_SURFACE('',#9163,0.24505);
#7974=ADVANCED_FACE('',(#1302),#927,.F.);
#7975=ADVANCED_FACE('',(#1303),#928,.F.);
#7976=ADVANCED_FACE('',(#1304),#929,.F.);
#7977=ADVANCED_FACE('',(#1305),#930,.F.);
#7978=ADVANCED_FACE('',(#1306),#931,.F.);
#7979=ADVANCED_FACE('',(#1307),#932,.F.);
#7980=ADVANCED_FACE('',(#1308),#933,.F.);
#7981=ADVANCED_FACE('',(#1309),#934,.F.);
#7982=ADVANCED_FACE('',(#1310),#935,.F.);
#7983=ADVANCED_FACE('',(#1311),#936,.T.);
#7984=ADVANCED_FACE('',(#1312),#406,.T.);
#7985=ADVANCED_FACE('',(#1313),#7687,.T.);
#7986=ADVANCED_FACE('',(#1314),#407,.T.);
#7987=ADVANCED_FACE('',(#1315,#719),#937,.T.);
#7988=ADVANCED_FACE('',(#1316),#408,.T.);
#7989=ADVANCED_FACE('',(#1317),#7688,.T.);
#8260=CLOSED_SHELL('',(#7974,#7975,#7976,#7977,#7978,#7979,#7980,#7981));
#8261=CLOSED_SHELL('',(#7982,#7983,#7984,#7985,#7986,#7987,#7988,#7989));
#9140=AXIS2_PLACEMENT_3D('',#13431,#10863,#10864);
#9141=AXIS2_PLACEMENT_3D('',#13432,#10865,#10866);
#9142=AXIS2_PLACEMENT_3D('',#13441,#10871,#10872);
#9143=AXIS2_PLACEMENT_3D('',#13447,#10876,#10877);
#9144=AXIS2_PLACEMENT_3D('',#13453,#10881,#10882);
#9145=AXIS2_PLACEMENT_3D('',#13459,#10886,#10887);
#9146=AXIS2_PLACEMENT_3D('',#13465,#10891,#10892);
#9147=AXIS2_PLACEMENT_3D('',#13468,#10895,#10896);
#9148=AXIS2_PLACEMENT_3D('',#13469,#10897,#10898);
#9149=AXIS2_PLACEMENT_3D('',#13470,#10899,#10900);
#9150=AXIS2_PLACEMENT_3D('',#13472,#10901,#10902);
#9151=AXIS2_PLACEMENT_3D('',#13473,#10903,#10904);
#9152=AXIS2_PLACEMENT_3D('',#13475,#10905,#10906);
#9153=AXIS2_PLACEMENT_3D('',#13476,#10907,#10908);
#9154=AXIS2_PLACEMENT_3D('',#13478,#10909,#10910);
#9155=AXIS2_PLACEMENT_3D('',#13480,#10912,#10913);
#9156=AXIS2_PLACEMENT_3D('',#13482,#10914,#10915);
#9157=AXIS2_PLACEMENT_3D('',#13484,#10917,#10918);
#9158=AXIS2_PLACEMENT_3D('',#13486,#10919,#10920);
#9159=AXIS2_PLACEMENT_3D('',#13488,#10922,#10923);
#9160=AXIS2_PLACEMENT_3D('',#13490,#10924,#10925);
#9161=AXIS2_PLACEMENT_3D('',#13491,#10926,#10927);
#9162=AXIS2_PLACEMENT_3D('',#13493,#10928,#10929);
#9163=AXIS2_PLACEMENT_3D('',#13495,#10931,#10932);
#10863=DIRECTION('axis',(0.,0.,1.));
#10864=DIRECTION('refdir',(1.,0.,0.));
#10865=DIRECTION('center_axis',(0.866025403784439,0.,-0.5));
#10866=DIRECTION('ref_axis',(0.5,0.,0.866025403784439));
#10867=DIRECTION('',(-0.5,0.,-0.866025403784439));
#10868=DIRECTION('',(0.,-1.,0.));
#10869=DIRECTION('',(0.5,0.,0.866025403784439));
#10870=DIRECTION('',(0.,-1.,0.));
#10871=DIRECTION('center_axis',(1.20185167898973E-16,0.,-1.));
#10872=DIRECTION('ref_axis',(1.,0.,1.20185167898973E-16));
#10873=DIRECTION('',(-1.,0.,-1.20185167898973E-16));
#10874=DIRECTION('',(0.,-1.,0.));
#10875=DIRECTION('',(1.,0.,1.20185167898973E-16));
#10876=DIRECTION('center_axis',(-0.866025403784439,0.,-0.5));
#10877=DIRECTION('ref_axis',(0.5,0.,-0.866025403784439));
#10878=DIRECTION('',(-0.5,0.,0.866025403784439));
#10879=DIRECTION('',(0.,-1.,0.));
#10880=DIRECTION('',(0.5,0.,-0.866025403784439));
#10881=DIRECTION('center_axis',(-0.866025403784439,0.,0.5));
#10882=DIRECTION('ref_axis',(-0.5,0.,-0.866025403784439));
#10883=DIRECTION('',(0.5,0.,0.866025403784439));
#10884=DIRECTION('',(0.,-1.,0.));
#10885=DIRECTION('',(-0.5,0.,-0.866025403784439));
#10886=DIRECTION('center_axis',(-2.40370335797945E-16,0.,1.));
#10887=DIRECTION('ref_axis',(-1.,0.,-2.40370335797945E-16));
#10888=DIRECTION('',(1.,0.,2.40370335797945E-16));
#10889=DIRECTION('',(0.,-1.,0.));
#10890=DIRECTION('',(-1.,0.,-2.40370335797945E-16));
#10891=DIRECTION('center_axis',(0.866025403784439,0.,0.5));
#10892=DIRECTION('ref_axis',(-0.5,0.,0.866025403784439));
#10893=DIRECTION('',(0.5,0.,-0.866025403784439));
#10894=DIRECTION('',(-0.5,0.,0.866025403784439));
#10895=DIRECTION('center_axis',(0.,1.,0.));
#10896=DIRECTION('ref_axis',(1.,0.,0.));
#10897=DIRECTION('center_axis',(0.,-1.,0.));
#10898=DIRECTION('ref_axis',(0.,0.,-1.));
#10899=DIRECTION('center_axis',(0.,1.,0.));
#10900=DIRECTION('ref_axis',(1.,0.,0.));
#10901=DIRECTION('center_axis',(0.,1.,0.));
#10902=DIRECTION('ref_axis',(1.,0.,0.));
#10903=DIRECTION('center_axis',(0.,1.,0.));
#10904=DIRECTION('ref_axis',(0.,0.,1.));
#10905=DIRECTION('center_axis',(0.,-1.,0.));
#10906=DIRECTION('ref_axis',(1.,0.,0.));
#10907=DIRECTION('center_axis',(0.,-1.,0.));
#10908=DIRECTION('ref_axis',(1.,0.,0.));
#10909=DIRECTION('center_axis',(0.,-1.,0.));
#10910=DIRECTION('ref_axis',(1.,0.,0.));
#10911=DIRECTION('',(0.707106781186548,0.707106781186547,8.65956056235493E-17));
#10912=DIRECTION('center_axis',(0.,-1.,0.));
#10913=DIRECTION('ref_axis',(1.,0.,0.));
#10914=DIRECTION('center_axis',(0.,-1.,0.));
#10915=DIRECTION('ref_axis',(1.,0.,0.));
#10916=DIRECTION('',(0.,1.,0.));
#10917=DIRECTION('center_axis',(0.,1.,0.));
#10918=DIRECTION('ref_axis',(1.,0.,0.));
#10919=DIRECTION('center_axis',(0.,-1.,0.));
#10920=DIRECTION('ref_axis',(1.,0.,0.));
#10921=DIRECTION('',(-0.707106781186547,0.707106781186548,-8.65956056235493E-17));
#10922=DIRECTION('center_axis',(0.,-1.,0.));
#10923=DIRECTION('ref_axis',(0.,0.,-1.));
#10924=DIRECTION('center_axis',(0.,-1.,0.));
#10925=DIRECTION('ref_axis',(1.,0.,0.));
#10926=DIRECTION('center_axis',(0.,1.,0.));
#10927=DIRECTION('ref_axis',(1.,0.,0.));
#10928=DIRECTION('center_axis',(0.,1.,0.));
#10929=DIRECTION('ref_axis',(1.,0.,0.));
#10930=DIRECTION('',(-0.447213595499958,0.894427190999916,-5.47678698264203E-17));
#10931=DIRECTION('center_axis',(0.,-1.,0.));
#10932=DIRECTION('ref_axis',(1.,0.,0.));
#10933=DIRECTION('',(0.,1.,0.));
#13431=CARTESIAN_POINT('',(0.,0.,0.));
#13432=CARTESIAN_POINT('Origin',(0.115470053837925,-0.5,-0.2));
#13433=CARTESIAN_POINT('',(0.23094010767585,-0.5,0.));
#13434=CARTESIAN_POINT('',(0.115470053837925,-0.5,-0.2));
#13435=CARTESIAN_POINT('',(0.23094010767585,-0.5,0.));
#13436=CARTESIAN_POINT('',(0.115470053837925,-0.8,-0.2));
#13437=CARTESIAN_POINT('',(0.115470053837925,-0.5,-0.2));
#13438=CARTESIAN_POINT('',(0.23094010767585,-0.8,0.));
#13439=CARTESIAN_POINT('',(0.23094010767585,-0.8,0.));
#13440=CARTESIAN_POINT('',(0.23094010767585,-0.5,0.));
#13441=CARTESIAN_POINT('Origin',(-0.115470053837925,-0.5,-0.2));
#13442=CARTESIAN_POINT('',(-0.115470053837925,-0.5,-0.2));
#13443=CARTESIAN_POINT('',(0.115470053837925,-0.5,-0.2));
#13444=CARTESIAN_POINT('',(-0.115470053837925,-0.8,-0.2));
#13445=CARTESIAN_POINT('',(-0.115470053837925,-0.5,-0.2));
#13446=CARTESIAN_POINT('',(0.115470053837925,-0.8,-0.2));
#13447=CARTESIAN_POINT('Origin',(-0.23094010767585,-0.5,-2.77555756156289E-17));
#13448=CARTESIAN_POINT('',(-0.23094010767585,-0.5,-2.82820063659975E-17));
#13449=CARTESIAN_POINT('',(-0.115470053837925,-0.5,-0.2));
#13450=CARTESIAN_POINT('',(-0.23094010767585,-0.8,-2.77555756156289E-17));
#13451=CARTESIAN_POINT('',(-0.23094010767585,-0.5,-2.82820063659975E-17));
#13452=CARTESIAN_POINT('',(-0.115470053837925,-0.8,-0.2));
#13453=CARTESIAN_POINT('Origin',(-0.115470053837925,-0.5,0.2));
#13454=CARTESIAN_POINT('',(-0.115470053837925,-0.5,0.2));
#13455=CARTESIAN_POINT('',(-0.23094010767585,-0.5,-2.82820063659975E-17));
#13456=CARTESIAN_POINT('',(-0.115470053837925,-0.8,0.2));
#13457=CARTESIAN_POINT('',(-0.115470053837925,-0.5,0.2));
#13458=CARTESIAN_POINT('',(-0.23094010767585,-0.8,-2.82820063659975E-17));
#13459=CARTESIAN_POINT('Origin',(0.115470053837925,-0.5,0.2));
#13460=CARTESIAN_POINT('',(0.115470053837925,-0.5,0.2));
#13461=CARTESIAN_POINT('',(-0.115470053837925,-0.5,0.2));
#13462=CARTESIAN_POINT('',(0.115470053837925,-0.8,0.2));
#13463=CARTESIAN_POINT('',(0.115470053837925,-0.5,0.2));
#13464=CARTESIAN_POINT('',(-0.115470053837925,-0.8,0.2));
#13465=CARTESIAN_POINT('Origin',(0.23094010767585,-0.5,0.));
#13466=CARTESIAN_POINT('',(0.115470053837925,-0.5,0.2));
#13467=CARTESIAN_POINT('',(0.115470053837925,-0.8,0.2));
#13468=CARTESIAN_POINT('Origin',(0.,-0.5,0.));
#13469=CARTESIAN_POINT('Origin',(0.,-0.8,0.));
#13470=CARTESIAN_POINT('Origin',(0.,-1.4,0.));
#13471=CARTESIAN_POINT('',(-0.24505,-1.4,3.00099698131059E-17));
#13472=CARTESIAN_POINT('Origin',(0.,-1.4,0.));
#13473=CARTESIAN_POINT('Origin',(0.375,0.5,0.));
#13474=CARTESIAN_POINT('',(-0.375,0.5,-4.59242549680257E-17));
#13475=CARTESIAN_POINT('Origin',(0.,0.5,0.));
#13476=CARTESIAN_POINT('Origin',(0.,0.475,0.));
#13477=CARTESIAN_POINT('',(-0.425,0.45,-5.20474889637625E-17));
#13478=CARTESIAN_POINT('Origin',(0.,0.45,0.));
#13479=CARTESIAN_POINT('',(-0.4,0.475,-4.89858719658941E-17));
#13480=CARTESIAN_POINT('Origin',(0.,0.24,0.));
#13481=CARTESIAN_POINT('',(-0.425,0.0299999999999998,-5.20474889637625E-17));
#13482=CARTESIAN_POINT('Origin',(0.,0.0299999999999998,0.));
#13483=CARTESIAN_POINT('',(-0.425,0.24,-5.20474889637625E-17));
#13484=CARTESIAN_POINT('Origin',(0.,0.0150000000000001,0.));
#13485=CARTESIAN_POINT('',(-0.395,4.85722573273506E-17,-4.83735485663204E-17));
#13486=CARTESIAN_POINT('Origin',(0.,0.,0.));
#13487=CARTESIAN_POINT('',(-0.41,0.0150000000000001,-5.02105187650415E-17));
#13488=CARTESIAN_POINT('Origin',(0.27,0.,0.));
#13489=CARTESIAN_POINT('',(-0.27,0.,-3.30654635769785E-17));
#13490=CARTESIAN_POINT('Origin',(0.,0.,0.));
#13491=CARTESIAN_POINT('Origin',(0.,-0.02,0.));
#13492=CARTESIAN_POINT('',(-0.24505,-0.0498999999999999,3.00099698131059E-17));
#13493=CARTESIAN_POINT('Origin',(0.,-0.0498999999999999,0.));
#13494=CARTESIAN_POINT('',(-0.26,-0.02,-3.18408167778312E-17));
#13495=CARTESIAN_POINT('Origin',(0.,-0.995,0.));
#13496=CARTESIAN_POINT('',(-0.24505,-0.995,-3.00099698131059E-17));
#15130=UNCERTAINTY_MEASURE_WITH_UNIT(LENGTH_MEASURE(0.001),#15213,
'DISTANCE_ACCURACY_VALUE',
'Maximum model space distance between geometric entities at asserted c
onnectivities');
#15162=UNCERTAINTY_MEASURE_WITH_UNIT(LENGTH_MEASURE(0.001),#15213,
'DISTANCE_ACCURACY_VALUE',
'Maximum model space distance between geometric entities at asserted c
onnectivities');
#15180=(
GEOMETRIC_REPRESENTATION_CONTEXT(3)
GLOBAL_UNCERTAINTY_ASSIGNED_CONTEXT((#15130))
GLOBAL_UNIT_ASSIGNED_CONTEXT((#15213,#15215,#15216))
REPRESENTATION_CONTEXT('','3D')
);
#15212=(
GEOMETRIC_REPRESENTATION_CONTEXT(3)
GLOBAL_UNCERTAINTY_ASSIGNED_CONTEXT((#15162))
GLOBAL_UNIT_ASSIGNED_CONTEXT((#15213,#15215,#15216))
REPRESENTATION_CONTEXT('','3D')
);
#15213=(
LENGTH_UNIT()
NAMED_UNIT(*)
SI_UNIT(.CENTI.,.METRE.)
);
#15215=(
NAMED_UNIT(*)
PLANE_ANGLE_UNIT()
SI_UNIT($,.RADIAN.)
);
#15216=(
NAMED_UNIT(*)
SI_UNIT($,.STERADIAN.)
SOLID_ANGLE_UNIT()
);
#15234=SHAPE_DEFINITION_REPRESENTATION(#15283,#15418);
#15283=PRODUCT_DEFINITION_SHAPE('',$,#15468);
#15418=SHAPE_REPRESENTATION('',(#9140),#15180);
#15450=PRODUCT_DEFINITION_CONTEXT('part definition',#15599,'design');
#15468=PRODUCT_DEFINITION('M5x14 Cap Screw','M5x14 Cap Screw',#15517,#15450);
#15517=PRODUCT_DEFINITION_FORMATION('',$,#15618);
#15599=APPLICATION_CONTEXT(
'Core Data for Automotive Mechanical Design Process');
#15600=PRODUCT_CONTEXT('part definition',#15599,'mechanical');
#15618=PRODUCT('M5x14 Cap Screw','M5x14 Cap Screw','M5x14 Cap Screw',(#15600));
#15720=COLOUR_RGB('Black',0.12,0.14,0.17);
#15721=FILL_AREA_STYLE_COLOUR('',#15720);
#15722=FILL_AREA_STYLE('',(#15721));
#15723=SURFACE_STYLE_FILL_AREA(#15722);
#15724=SURFACE_SIDE_STYLE('',(#15723));
#15725=SURFACE_STYLE_USAGE(.BOTH.,#15724);
#15726=PRESENTATION_STYLE_ASSIGNMENT((#15725));
ENDSEC;
END-ISO-10303-21;
